ISO-10303-21;
HEADER;
FILE_DESCRIPTION (('STEP AP214'),
    '1' );
FILE_NAME ('Handle Mounting Screw.step',
    '2026-10-06T09:49:54',
    ( '' ),
    ( '' ),
    'SwSTEP 2.0',
    'SolidWorks 2020',
    '' );
FILE_SCHEMA (( 'AUTOMOTIVE_DESIGN' ));
ENDSEC;

DATA;
#303=CIRCLE ( 'NONE', #93224, 4.820754716980014010 ) ;
#652=CARTESIAN_POINT ( 'NONE',  ( -113.4000000000000057, 1392.913060387289988, 304.2218459572590064 ) ) ;
#909=CIRCLE ( 'NONE', #106386, 2.500000000000002220 ) ;
#969=PRESENTATION_STYLE_ASSIGNMENT (( #77656 ) ) ;
#1390=ORIENTED_EDGE ( 'NONE', *, *, #83101, .T. ) ;
#1499=ADVANCED_FACE ( 'NONE', ( #70628 ), #95038, .T. ) ;
#1513=( NAMED_UNIT ( * ) SI_UNIT ( $, .STERADIAN. ) SOLID_ANGLE_UNIT ( ) );
#1709=CARTESIAN_POINT ( 'NONE',  ( -114.7007400580323520, 1391.413060387289988, 302.0868810157617190 ) ) ;
#1762=DIRECTION ( 'NONE',  ( -0.5202960232132588514, 0.000000000000000000, -0.8539859765994216589 ) ) ;
#2388=ORIENTED_EDGE ( 'NONE', *, *, #77734, .T. ) ;
#2559=DIRECTION ( 'NONE',  ( 0.3188159025760192167, 6.661338147751048295E-13, -0.9478166596260261256 ) ) ;
#3431=FACE_OUTER_BOUND ( 'NONE', #16047, .T. ) ;
#4282=DIRECTION ( 'NONE',  ( 0.000000000000000000, -1.000000000000000000, 0.000000000000000000 ) ) ;
#5350=ORIENTED_EDGE ( 'NONE', *, *, #15257, .T. ) ;
#5539=FACE_OUTER_BOUND ( 'NONE', #71299, .T. ) ;
#5590=CARTESIAN_POINT ( 'NONE',  ( -113.4000000000000057, 1391.413060387289988, 304.2218459572590064 ) ) ;
#5634=DIRECTION ( 'NONE',  ( -0.3679048462383226470, -0.7071067811868645414, -0.6038592750913974738 ) ) ;
#6353=CARTESIAN_POINT ( 'NONE',  ( -113.4000000000000057, 1347.163060387289988, 304.2218459572590064 ) ) ;
#6510=VERTEX_POINT ( 'NONE', #25737 ) ;
#6621=VERTEX_POINT ( 'NONE', #69811 ) ;
#6634=DIRECTION ( 'NONE',  ( 0.000000000000000000, 0.000000000000000000, -1.000000000000000000 ) ) ;
#6719=LINE ( 'NONE', #106436, #50337 ) ;
#6879=EDGE_CURVE ( 'NONE', #43545, #22154, #58072, .T. ) ;
#7095=TOROIDAL_SURFACE ( 'NONE', #69718, 3.000000000000000000, 0.5000000000000000000 ) ;
#7472=CARTESIAN_POINT ( 'NONE',  ( -116.0368005749632943, 1305.714868215269917, 309.0484770343335867 ) ) ;
#7851=DIRECTION ( 'NONE',  ( 0.000000000000000000, 0.000000000000000000, 1.000000000000000000 ) ) ;
#7937=MANIFOLD_SOLID_BREP ( 'Stock-MAS-682-1', #35981 ) ;
#8026=VERTEX_POINT ( 'NONE', #16602 ) ;
#8115=CARTESIAN_POINT ( 'NONE',  ( -113.4000000000000057, 1391.413060387289988, 304.2218459572590064 ) ) ;
#8417=DIRECTION ( 'NONE',  ( 0.000000000000000000, 0.000000000000000000, 1.000000000000000000 ) ) ;
#8868=DIRECTION ( 'NONE',  ( 0.3188159025760192167, 6.661338147751048295E-13, -0.9478166596260261256 ) ) ;
#8888=ORIENTED_EDGE ( 'NONE', *, *, #30536, .T. ) ;
#8970=PLANE ( 'NONE',  #41264 ) ;
#9125=AXIS2_PLACEMENT_3D ( 'NONE', #43513, #75997, #92794 ) ;
#9144=ORIENTED_EDGE ( 'NONE', *, *, #30536, .F. ) ;
#9180=ORIENTED_EDGE ( 'NONE', *, *, #94626, .F. ) ;
#9664=SPHERICAL_SURFACE ( 'NONE', #90796, 7.299999999999999822 ) ;
#9858=DIRECTION ( 'NONE',  ( 0.4794255386041804123, 0.000000000000000000, -0.8775825618903850822 ) ) ;
#10350=DIRECTION ( 'NONE',  ( 0.4794255386042096112, 0.000000000000000000, -0.8775825618903690950 ) ) ;
#10448=FILL_AREA_STYLE_COLOUR ( '', #31521 ) ;
#10461=ORIENTED_EDGE ( 'NONE', *, *, #65289, .T. ) ;
#10690=VERTEX_POINT ( 'NONE', #56968 ) ;
#10944=PRESENTATION_STYLE_ASSIGNMENT (( #104998 ) ) ;
#11604=DIRECTION ( 'NONE',  ( -0.4794255386042071132, 0.000000000000000000, 0.8775825618903705383 ) ) ;
#12038=SHAPE_REPRESENTATION_RELATIONSHIP ( 'NONE' , 'NONE' ,  #110199, #100095 ) ;
#12218=CIRCLE ( 'NONE', #19325, 2.500000000000002220 ) ;
#12293=VECTOR ( 'NONE', #37518, 1000.000000000000000 ) ;
#12415=EDGE_LOOP ( 'NONE', ( #21183, #8888, #105550, #2388, #110528 ) ) ;
#12418=CARTESIAN_POINT ( 'NONE',  ( -112.3594079535740207, 1391.913060387289988, 305.9298179104569613 ) ) ;
#12997=ORIENTED_EDGE ( 'NONE', *, *, #102214, .F. ) ;
#13372=CIRCLE ( 'NONE', #75981, 5.499916801759985319 ) ;
#13526=AXIS2_PLACEMENT_3D ( 'NONE', #105789, #48078, #29603 ) ;
#14471=PLANE ( 'NONE',  #105479 ) ;
#14526=ADVANCED_FACE ( 'NONE', ( #3431 ), #78469, .T. ) ;
#14831=DIRECTION ( 'NONE',  ( -0.8775825618903712044, 0.000000000000000000, -0.4794255386042061140 ) ) ;
#14896=FACE_OUTER_BOUND ( 'NONE', #39182, .T. ) ;
#15257=EDGE_CURVE ( 'NONE', #102542, #76097, #6719, .T. ) ;
#15764=AXIS2_PLACEMENT_3D ( 'NONE', #87082, #102749, #2559 ) ;
#15912=EDGE_CURVE ( 'NONE', #67505, #32529, #303, .T. ) ;
#16047=EDGE_LOOP ( 'NONE', ( #107356, #28800, #21253 ) ) ;
#16538=DIRECTION ( 'NONE',  ( 0.000000000000000000, 0.000000000000000000, 1.000000000000000000 ) ) ;
#16602=CARTESIAN_POINT ( 'NONE',  ( -114.8382766158126174, 1305.913060387289988, 306.8545936429301264 ) ) ;
#17033=CIRCLE ( 'NONE', #49300, 2.000000000000001776 ) ;
#17086=EDGE_CURVE ( 'NONE', #8026, #57348, #52945, .T. ) ;
#17411=DIRECTION ( 'NONE',  ( 0.000000000000000000, 1.000000000000000000, 0.000000000000000000 ) ) ;
#17710=SURFACE_SIDE_STYLE ('',( #69276 ) ) ;
#18049=CARTESIAN_POINT ( 'NONE',  ( -113.7188159025760115, 1310.214785017039276, 305.1696626168879902 ) ) ;
#18801=AXIS2_PLACEMENT_3D ( 'NONE', #103083, #17411, #78461 ) ;
#19311=FILL_AREA_STYLE ('',( #41775 ) ) ;
#19325=AXIS2_PLACEMENT_3D ( 'NONE', #8115, #93758, #76432 ) ;
#19473=CARTESIAN_POINT ( 'NONE',  ( -114.4405920464259765, 1391.913060387289988, 302.5138740040609946 ) ) ;
#20018=ORIENTED_EDGE ( 'NONE', *, *, #68636, .F. ) ;
#20044=DIRECTION ( 'NONE',  ( 0.000000000000000000, -1.000000000000000000, 0.000000000000000000 ) ) ;
#20167=ORIENTED_EDGE ( 'NONE', *, *, #97888, .F. ) ;
#20300=ORIENTED_EDGE ( 'NONE', *, *, #38384, .F. ) ;
#20417=( NAMED_UNIT ( * ) PLANE_ANGLE_UNIT ( ) SI_UNIT ( $, .RADIAN. ) );
#21183=ORIENTED_EDGE ( 'NONE', *, *, #15912, .F. ) ;
#21193=DIRECTION ( 'NONE',  ( 0.000000000000000000, -1.000000000000000000, 0.000000000000000000 ) ) ;
#21253=ORIENTED_EDGE ( 'NONE', *, *, #54007, .T. ) ;
#21632=AXIS2_PLACEMENT_3D ( 'NONE', #110085, #42890, #42328 ) ;
#21747=DIRECTION ( 'NONE',  ( -0.8775825618903733139, -0.000000000000000000, -0.4794255386042020062 ) ) ;
#22047=DIRECTION ( 'NONE',  ( 0.000000000000000000, 0.000000000000000000, 1.000000000000000000 ) ) ;
#22154=VERTEX_POINT ( 'NONE', #78778 ) ;
#22443=ADVANCED_FACE ( 'NONE', ( #14896 ), #69456, .T. ) ;
#22662=CARTESIAN_POINT ( 'NONE',  ( -115.7111929266684882, 1304.231242809270043, 308.4524562320341943 ) ) ;
#23234=CARTESIAN_POINT ( 'NONE',  ( -113.4000000000000057, 1305.913060387289988, 304.2218459572590064 ) ) ;
#23373=EDGE_LOOP ( 'NONE', ( #35191, #20300 ) ) ;
#23419=DIRECTION ( 'NONE',  ( -0.4794255386041804123, 0.000000000000000000, 0.8775825618903850822 ) ) ;
#23869=CARTESIAN_POINT ( 'NONE',  ( -113.4000000000000057, 1391.913060387289988, 304.2218459572590064 ) ) ;
#23874=CARTESIAN_POINT ( 'NONE',  ( -112.2014361534894817, 1391.413060387289988, 302.0278895525330540 ) ) ;
#24075=AXIS2_PLACEMENT_3D ( 'NONE', #23234, #41152, #75861 ) ;
#24087=CARTESIAN_POINT ( 'NONE',  ( -113.4000000000000057, 1391.413060387289988, 304.2218459572590064 ) ) ;
#24123=ORIENTED_EDGE ( 'NONE', *, *, #17086, .F. ) ;
#24237=FACE_OUTER_BOUND ( 'NONE', #61136, .T. ) ;
#24331=EDGE_CURVE ( 'NONE', #94097, #57348, #101047, .T. ) ;
#24463=CIRCLE ( 'NONE', #29906, 5.499916801759985319 ) ;
#24520=AXIS2_PLACEMENT_3D ( 'NONE', #98479, #21747, #96852 ) ;
#24559=DIRECTION ( 'NONE',  ( 0.000000000000000000, -1.000000000000000000, 0.000000000000000000 ) ) ;
#25106=ADVANCED_FACE ( 'NONE', ( #46848 ), #80977, .T. ) ;
#25522=ADVANCED_FACE ( 'NONE', ( #97904 ), #65440, .T. ) ;
#25532=CARTESIAN_POINT ( 'NONE',  ( -112.8797039767867432, 1392.913060387289988, 305.0758319338584101 ) ) ;
#25572=UNCERTAINTY_MEASURE_WITH_UNIT (LENGTH_MEASURE( 1.000000000000000082E-05 ), #80901, 'distance_accuracy_value', 'NONE');
#25617=FACE_OUTER_BOUND ( 'NONE', #52288, .T. ) ;
#25737=CARTESIAN_POINT ( 'NONE',  ( -115.1534609392471395, 1305.714868215269917, 309.4347587285261625 ) ) ;
#25954=ORIENTED_EDGE ( 'NONE', *, *, #77734, .F. ) ;
#26147=( GEOMETRIC_REPRESENTATION_CONTEXT ( 3 ) GLOBAL_UNCERTAINTY_ASSIGNED_CONTEXT ( ( #26688 ) ) GLOBAL_UNIT_ASSIGNED_CONTEXT ( ( #110698, #26686, #1513 ) ) REPRESENTATION_CONTEXT ( 'NONE', 'WORKASPACE' ) );
#26663=ORIENTED_EDGE ( 'NONE', *, *, #94626, .T. ) ;
#26686=( NAMED_UNIT ( * ) PLANE_ANGLE_UNIT ( ) SI_UNIT ( $, .RADIAN. ) );
#26688=UNCERTAINTY_MEASURE_WITH_UNIT (LENGTH_MEASURE( 1.000000000000000082E-05 ), #110698, 'distance_accuracy_value', 'NONE');
#26795=DIRECTION ( 'NONE',  ( 0.000000000000000000, 0.000000000000000000, 1.000000000000000000 ) ) ;
#28022=ORIENTED_EDGE ( 'NONE', *, *, #43399, .T. ) ;
#28168=ORIENTED_EDGE ( 'NONE', *, *, #36962, .T. ) ;
#28297=EDGE_CURVE ( 'NONE', #96166, #6510, #13372, .T. ) ;
#28440=DIRECTION ( 'NONE',  ( -0.5202960232132588514, 0.000000000000000000, -0.8539859765994216589 ) ) ;
#28605=CONICAL_SURFACE ( 'NONE', #91183, 0.9999999999999836797, 0.7853981633970000820 ) ;
#28800=ORIENTED_EDGE ( 'NONE', *, *, #15912, .T. ) ;
#28861=EDGE_CURVE ( 'NONE', #102542, #43545, #17033, .T. ) ;
#28864=MECHANICAL_DESIGN_GEOMETRIC_PRESENTATION_REPRESENTATION('',(#68204),#39564);
#29603=DIRECTION ( 'NONE',  ( -0.4794255386042071132, 0.000000000000000000, 0.8775825618903705383 ) ) ;
#29661=LINE ( 'NONE', #108015, #12293 ) ;
#29664=DIRECTION ( 'NONE',  ( 0.000000000000000000, -1.000000000000000000, 0.000000000000000000 ) ) ;
#29906=AXIS2_PLACEMENT_3D ( 'NONE', #33823, #68015, #102125 ) ;
#30076=DIRECTION ( 'NONE',  ( 0.000000000000000000, 0.000000000000000000, 1.000000000000000000 ) ) ;
#30140=CIRCLE ( 'NONE', #92737, 2.500000000000002220 ) ;
#30536=EDGE_CURVE ( 'NONE', #67505, #96166, #50886, .T. ) ;
#30569=DIRECTION ( 'NONE',  ( -0.4794255386042076128, 0.000000000000000000, 0.8775825618903700942 ) ) ;
#30684=EDGE_CURVE ( 'NONE', #8026, #87268, #56491, .T. ) ;
#31180=CIRCLE ( 'NONE', #104478, 5.499916801759985319 ) ;
#31203=EDGE_CURVE ( 'NONE', #106581, #6621, #72410, .T. ) ;
#31454=AXIS2_PLACEMENT_3D ( 'NONE', #83410, #58776, #92914 ) ;
#31521=COLOUR_RGB ( '', 0.66274510, 0.83137255, 0.94901961) ;
#31881=DIRECTION ( 'NONE',  ( 0.000000000000000000, -1.000000000000000000, 0.000000000000000000 ) ) ;
#32019=APPLICATION_CONTEXT ( 'automotive_design' ) ;
#32529=VERTEX_POINT ( 'NONE', #22662 ) ;
#33107=ORIENTED_EDGE ( 'NONE', *, *, #38384, .T. ) ;
#33736=LINE ( 'NONE', #34850, #80015 ) ;
#33823=CARTESIAN_POINT ( 'NONE',  ( -113.4000000000000057, 1305.714868215269917, 304.2218459572590064 ) ) ;
#33917=( LENGTH_UNIT ( ) NAMED_UNIT ( * ) SI_UNIT ( .MILLI., .METRE. ) );
#34176=DIRECTION ( 'NONE',  ( 0.000000000000000000, -1.000000000000000000, 0.000000000000000000 ) ) ;
#34194=COLOUR_RGB ( '', 0.66274510, 0.83137255, 0.94901961) ;
#34237=AXIS2_PLACEMENT_3D ( 'NONE', #110010, #40043, #91555 ) ;
#34639=ORIENTED_EDGE ( 'NONE', *, *, #36962, .F. ) ;
#34850=CARTESIAN_POINT ( 'NONE',  ( -113.0811840974239857, 1310.214785017040640, 303.2740292976359910 ) ) ;
#35191=ORIENTED_EDGE ( 'NONE', *, *, #31203, .F. ) ;
#35356=DIRECTION ( 'NONE',  ( -0.8775825618903734249, -0.000000000000000000, -0.4794255386042018952 ) ) ;
#35981=CLOSED_SHELL ( 'NONE', ( #98514, #70721, #25522, #77445, #41435, #1499, #99311, #25106, #56976, #22443, #89036, #42049, #57866, #14526 ) ) ;
#36017=AXIS2_PLACEMENT_3D ( 'NONE', #89891, #108906, #66925 ) ;
#36377=CARTESIAN_POINT ( 'NONE',  ( -112.2014361534894817, 1347.163060387289988, 302.0278895525330540 ) ) ;
#36533=DIRECTION ( 'NONE',  ( -0.8775825618903734249, -0.000000000000000000, -0.4794255386042018952 ) ) ;
#36962=EDGE_CURVE ( 'NONE', #76097, #60628, #84956, .T. ) ;
#36982=DIRECTION ( 'NONE',  ( -2.220446049250000002E-16, -1.000000000000000000, 2.220446049250000002E-16 ) ) ;
#37081=DIRECTION ( 'NONE',  ( -0.4794255386042018952, 0.000000000000000000, 0.8775825618903733139 ) ) ;
#37518=DIRECTION ( 'NONE',  ( 0.000000000000000000, -1.000000000000000000, 0.000000000000000000 ) ) ;
#38384=EDGE_CURVE ( 'NONE', #6621, #106581, #110147, .T. ) ;
#38630=VECTOR ( 'NONE', #50227, 1000.000000000000000 ) ;
#38682=PRODUCT_DEFINITION_FORMATION_WITH_SPECIFIED_SOURCE ( 'ANY', '', #71492, .NOT_KNOWN. ) ;
#39182=EDGE_LOOP ( 'NONE', ( #63984, #33107, #75082, #92151, #25954 ) ) ;
#39205=AXIS2_PLACEMENT_3D ( 'NONE', #44325, #35356, #70102 ) ;
#39564=( GEOMETRIC_REPRESENTATION_CONTEXT ( 3 ) GLOBAL_UNCERTAINTY_ASSIGNED_CONTEXT ( ( #25572 ) ) GLOBAL_UNIT_ASSIGNED_CONTEXT ( ( #80901, #20417, #88204 ) ) REPRESENTATION_CONTEXT ( 'NONE', 'WORKASPACE' ) );
#39875=APPLICATION_CONTEXT ( 'automotive_design' ) ;
#40043=DIRECTION ( 'NONE',  ( 0.8775825618903732028, 0.000000000000000000, 0.4794255386042021172 ) ) ;
#40092=EDGE_LOOP ( 'NONE', ( #9144, #20018, #71301, #82952, #70487 ) ) ;
#40691=AXIS2_PLACEMENT_3D ( 'NONE', #79949, #54221, #28440 ) ;
#41152=DIRECTION ( 'NONE',  ( 0.000000000000000000, -1.000000000000000000, 0.000000000000000000 ) ) ;
#41160=ORIENTED_EDGE ( 'NONE', *, *, #63318, .F. ) ;
#41264=AXIS2_PLACEMENT_3D ( 'NONE', #100283, #34176, #41489 ) ;
#41370=DIRECTION ( 'NONE',  ( 0.000000000000000000, -1.000000000000000000, 0.000000000000000000 ) ) ;
#41435=ADVANCED_FACE ( 'NONE', ( #24237 ), #93103, .T. ) ;
#41489=DIRECTION ( 'NONE',  ( 0.000000000000000000, 0.000000000000000000, -1.000000000000000000 ) ) ;
#41524=PRODUCT_CONTEXT ( 'NONE', #32019, 'mechanical' ) ;
#41775=FILL_AREA_STYLE_COLOUR ( '', #34194 ) ;
#41802=DIRECTION ( 'NONE',  ( 0.8775825618903713154, 0.000000000000000000, 0.4794255386042060030 ) ) ;
#41940=FACE_OUTER_BOUND ( 'NONE', #43328, .T. ) ;
#41972=CARTESIAN_POINT ( 'NONE',  ( -111.7220106148852778, 1305.733110638860126, 301.1503069906427186 ) ) ;
#42049=ADVANCED_FACE ( 'NONE', ( #46882 ), #96407, .T. ) ;
#42328=DIRECTION ( 'NONE',  ( 1.000000000000000000, 0.000000000000000000, 0.000000000000000000 ) ) ;
#42604=EDGE_CURVE ( 'NONE', #60628, #22154, #12218, .T. ) ;
#42890=DIRECTION ( 'NONE',  ( 0.000000000000000000, 0.000000000000000000, 1.000000000000000000 ) ) ;
#43000=AXIS2_PLACEMENT_3D ( 'NONE', #81271, #94637, #8417 ) ;
#43328=EDGE_LOOP ( 'NONE', ( #44001, #28022, #76675, #58449, #70782 ) ) ;
#43399=EDGE_CURVE ( 'NONE', #6621, #6510, #61754, .T. ) ;
#43513=CARTESIAN_POINT ( 'NONE',  ( -113.4000000000000057, 1306.413060387289988, 304.2218459572590064 ) ) ;
#43545=VERTEX_POINT ( 'NONE', #12418 ) ;
#43604=EDGE_LOOP ( 'NONE', ( #90192, #109547, #105668 ) ) ;
#44001=ORIENTED_EDGE ( 'NONE', *, *, #31203, .T. ) ;
#44325=CARTESIAN_POINT ( 'NONE',  ( -113.4000000000000057, 1309.713060387289943, 304.2218459572590064 ) ) ;
#44485=VERTEX_POINT ( 'NONE', #109535 ) ;
#45054=ORIENTED_EDGE ( 'NONE', *, *, #30684, .F. ) ;
#45122=ORIENTED_EDGE ( 'NONE', *, *, #63318, .T. ) ;
#45399=CARTESIAN_POINT ( 'NONE',  ( -113.4000000000000057, 1391.413060387289988, 304.2218459572590064 ) ) ;
#45568=VERTEX_POINT ( 'NONE', #55018 ) ;
#46848=FACE_OUTER_BOUND ( 'NONE', #70009, .T. ) ;
#46882=FACE_OUTER_BOUND ( 'NONE', #40092, .T. ) ;
#47259=VECTOR ( 'NONE', #21193, 1000.000000000000000 ) ;
#48078=DIRECTION ( 'NONE',  ( 0.000000000000000000, 1.000000000000000000, 0.000000000000000000 ) ) ;
#49020=DIRECTION ( 'NONE',  ( -0.4794255386042027833, 0.000000000000000000, 0.8775825618903728698 ) ) ;
#49210=DIRECTION ( 'NONE',  ( 0.000000000000000000, -1.000000000000000000, 0.000000000000000000 ) ) ;
#49300=AXIS2_PLACEMENT_3D ( 'NONE', #23869, #58065, #30076 ) ;
#49340=ORIENTED_EDGE ( 'NONE', *, *, #6879, .F. ) ;
#50227=DIRECTION ( 'NONE',  ( 0.3679048462383223694, -0.7071067811868645414, 0.6038592750913975848 ) ) ;
#50337=VECTOR ( 'NONE', #5634, 1000.000000000000000 ) ;
#50450=FACE_BOUND ( 'NONE', #103632, .T. ) ;
#50886=CIRCLE ( 'NONE', #79764, 2.000000000000023537 ) ;
#51562=ORIENTED_EDGE ( 'NONE', *, *, #30684, .T. ) ;
#52288=EDGE_LOOP ( 'NONE', ( #92458, #84615, #107518, #20167 ) ) ;
#52710=ORIENTED_EDGE ( 'NONE', *, *, #97888, .T. ) ;
#52770=AXIS2_PLACEMENT_3D ( 'NONE', #62653, #20044, #26795 ) ;
#52945=CIRCLE ( 'NONE', #95846, 0.5000000000000147660 ) ;
#52973=MECHANICAL_DESIGN_GEOMETRIC_PRESENTATION_REPRESENTATION('',(#60162),#26147);
#53597=CARTESIAN_POINT ( 'NONE',  ( -113.4000000000000057, 1347.163060387289988, 304.2218459572590064 ) ) ;
#53705=AXIS2_PLACEMENT_3D ( 'NONE', #100697, #41370, #99040 ) ;
#53718=EDGE_CURVE ( 'NONE', #87268, #8026, #71865, .T. ) ;
#54007=EDGE_CURVE ( 'NONE', #32529, #45568, #93217, .T. ) ;
#54069=EDGE_CURVE ( 'NONE', #32529, #57665, #62918, .T. ) ;
#54079=SURFACE_STYLE_FILL_AREA ( #19311 ) ;
#54221=DIRECTION ( 'NONE',  ( -2.220446049250000002E-16, -1.000000000000000000, 2.220446049250000002E-16 ) ) ;
#55018=CARTESIAN_POINT ( 'NONE',  ( -113.4000000000000057, 1302.413060387289988, 304.2218459572590064 ) ) ;
#56381=AXIS2_PLACEMENT_3D ( 'NONE', #24087, #66146, #7851 ) ;
#56491=CIRCLE ( 'NONE', #31454, 3.000000000000002665 ) ;
#56968=CARTESIAN_POINT ( 'NONE',  ( -111.6465390607511097, 1305.714868215269917, 299.0089331859842332 ) ) ;
#56976=ADVANCED_FACE ( 'NONE', ( #5539 ), #14471, .F. ) ;
#57348=VERTEX_POINT ( 'NONE', #101092 ) ;
#57665=VERTEX_POINT ( 'NONE', #7472 ) ;
#57866=ADVANCED_FACE ( 'NONE', ( #66037 ), #82275, .F. ) ;
#58065=DIRECTION ( 'NONE',  ( 0.000000000000000000, -1.000000000000000000, 0.000000000000000000 ) ) ;
#58072=LINE ( 'NONE', #25532, #38630 ) ;
#58449=ORIENTED_EDGE ( 'NONE', *, *, #93867, .F. ) ;
#58693=ORIENTED_EDGE ( 'NONE', *, *, #24331, .T. ) ;
#58776=DIRECTION ( 'NONE',  ( 0.000000000000000000, 1.000000000000000000, 0.000000000000000000 ) ) ;
#59155=CARTESIAN_POINT ( 'NONE',  ( -113.4000000000000057, 1305.714868215269917, 304.2218459572590064 ) ) ;
#59542=CARTESIAN_POINT ( 'NONE',  ( -113.4000000000000057, 1305.714868215269917, 304.2218459572590064 ) ) ;
#60162=STYLED_ITEM ( 'NONE', ( #969 ), #7937 ) ;
#60247=( NAMED_UNIT ( * ) SI_UNIT ( $, .STERADIAN. ) SOLID_ANGLE_UNIT ( ) );
#60628=VERTEX_POINT ( 'NONE', #23874 ) ;
#61136=EDGE_LOOP ( 'NONE', ( #28168, #10461, #58693, #12997, #45122 ) ) ;
#61475=CARTESIAN_POINT ( 'NONE',  ( -113.4000000000000057, 1305.733110638860126, 304.2218459572590064 ) ) ;
#61754=LINE ( 'NONE', #18049, #67638 ) ;
#62474=AXIS2_PLACEMENT_3D ( 'NONE', #6353, #84698, #108812 ) ;
#62653=CARTESIAN_POINT ( 'NONE',  ( -113.4000000000000057, 1391.913060387289988, 304.2218459572590064 ) ) ;
#62760=ORIENTED_EDGE ( 'NONE', *, *, #102214, .T. ) ;
#62895=CARTESIAN_POINT ( 'NONE',  ( -113.4000000000000057, 1309.713060387289943, 304.2218459572590064 ) ) ;
#62918=CIRCLE ( 'NONE', #89623, 2.000000000000023537 ) ;
#63318=EDGE_CURVE ( 'NONE', #44485, #76097, #909, .T. ) ;
#63708=EDGE_CURVE ( 'NONE', #43545, #102542, #77779, .T. ) ;
#63984=ORIENTED_EDGE ( 'NONE', *, *, #43399, .F. ) ;
#64667=CARTESIAN_POINT ( 'NONE',  ( -113.4000000000000057, 1305.913060387289988, 304.2218459572590064 ) ) ;
#65289=EDGE_CURVE ( 'NONE', #60628, #94097, #88444, .T. ) ;
#65372=AXIS2_PLACEMENT_3D ( 'NONE', #53597, #4282, #30569 ) ;
#65440=TOROIDAL_SURFACE ( 'NONE', #13526, 3.500000000000000000, 2.000000000000000000 ) ;
#65494=EDGE_CURVE ( 'NONE', #57665, #10690, #31180, .T. ) ;
#65722=CIRCLE ( 'NONE', #24520, 7.300000000000009592 ) ;
#65800=CONICAL_SURFACE ( 'NONE', #40691, 0.9999999999999910072, 0.7853981633970000820 ) ;
#66037=FACE_OUTER_BOUND ( 'NONE', #69351, .T. ) ;
#66146=DIRECTION ( 'NONE',  ( 0.000000000000000000, -1.000000000000000000, 0.000000000000000000 ) ) ;
#66543=AXIS2_PLACEMENT_3D ( 'NONE', #59155, #110086, #16538 ) ;
#66564=ORIENTED_EDGE ( 'NONE', *, *, #83101, .F. ) ;
#66568=CARTESIAN_POINT ( 'NONE',  ( -111.9617233841873940, 1306.413060387289988, 301.5890982715878863 ) ) ;
#66622=CARTESIAN_POINT ( 'NONE',  ( -113.4000000000000057, 1305.714868215269917, 304.2218459572590064 ) ) ;
#66925=DIRECTION ( 'NONE',  ( 0.000000000000000000, 0.000000000000000000, 1.000000000000000000 ) ) ;
#67071=UNCERTAINTY_MEASURE_WITH_UNIT (LENGTH_MEASURE( 1.000000000000000082E-05 ), #33917, 'distance_accuracy_value', 'NONE');
#67478=CARTESIAN_POINT ( 'NONE',  ( -115.0779893851147193, 1305.733110638860126, 307.2933849238752373 ) ) ;
#67505=VERTEX_POINT ( 'NONE', #91318 ) ;
#67638=VECTOR ( 'NONE', #86924, 1000.000000000000000 ) ;
#67808=CARTESIAN_POINT ( 'NONE',  ( -111.7097258769571368, 1305.913060387289988, 299.1967830284323782 ) ) ;
#67958=DIRECTION ( 'NONE',  ( 0.000000000000000000, -1.000000000000000000, 0.000000000000000000 ) ) ;
#68015=DIRECTION ( 'NONE',  ( 0.000000000000000000, -1.000000000000000000, 0.000000000000000000 ) ) ;
#68204=STYLED_ITEM ( 'NONE', ( #10944 ), #100095 ) ;
#68597=CARTESIAN_POINT ( 'NONE',  ( -113.4000000000000057, 1304.231242809270043, 304.2218459572590064 ) ) ;
#68636=EDGE_CURVE ( 'NONE', #32529, #67505, #100214, .T. ) ;
#69276=SURFACE_STYLE_FILL_AREA ( #110149 ) ;
#69351=EDGE_LOOP ( 'NONE', ( #24123, #51562, #52710, #9180 ) ) ;
#69456=CONICAL_SURFACE ( 'NONE', #15764, 0.9999999999999836797, 0.7853981633970000820 ) ;
#69718=AXIS2_PLACEMENT_3D ( 'NONE', #76046, #110190, #10350 ) ;
#69811=CARTESIAN_POINT ( 'NONE',  ( -115.0902741230411692, 1305.913060387289988, 309.2469088860785860 ) ) ;
#70009=EDGE_LOOP ( 'NONE', ( #103015, #103001, #1390, #62760, #26663 ) ) ;
#70053=ORIENTED_EDGE ( 'NONE', *, *, #63708, .F. ) ;
#70102=DIRECTION ( 'NONE',  ( -0.4794255386042018952, 0.000000000000000000, 0.8775825618903733139 ) ) ;
#70487=ORIENTED_EDGE ( 'NONE', *, *, #93867, .T. ) ;
#70628=FACE_OUTER_BOUND ( 'NONE', #77491, .T. ) ;
#70721=ADVANCED_FACE ( 'NONE', ( #25617 ), #7095, .F. ) ;
#70782=ORIENTED_EDGE ( 'NONE', *, *, #97665, .F. ) ;
#71299=EDGE_LOOP ( 'NONE', ( #98666, #70053 ) ) ;
#71301=ORIENTED_EDGE ( 'NONE', *, *, #54069, .T. ) ;
#71492=PRODUCT ( 'Handle Mounting Screw', 'Handle Mounting Screw', '', ( #41524 ) ) ;
#71865=CIRCLE ( 'NONE', #36017, 3.000000000000002665 ) ;
#72391=PRODUCT_DEFINITION_SHAPE ( 'NONE', 'NONE',  #82922 ) ;
#72410=CIRCLE ( 'NONE', #24075, 5.301724629749982043 ) ;
#75082=ORIENTED_EDGE ( 'NONE', *, *, #97665, .T. ) ;
#75861=DIRECTION ( 'NONE',  ( 0.000000000000000000, 0.000000000000000000, 1.000000000000000000 ) ) ;
#75981=AXIS2_PLACEMENT_3D ( 'NONE', #66622, #24559, #110240 ) ;
#75997=DIRECTION ( 'NONE',  ( 0.000000000000000000, 1.000000000000000000, 0.000000000000000000 ) ) ;
#76046=CARTESIAN_POINT ( 'NONE',  ( -113.4000000000000057, 1306.413060387289988, 304.2218459572590064 ) ) ;
#76097=VERTEX_POINT ( 'NONE', #1709 ) ;
#76432=DIRECTION ( 'NONE',  ( 0.000000000000000000, 0.000000000000000000, 1.000000000000000000 ) ) ;
#76671=DIRECTION ( 'NONE',  ( 0.8775825618903710934, -0.000000000000000000, 0.4794255386042062250 ) ) ;
#76675=ORIENTED_EDGE ( 'NONE', *, *, #28297, .F. ) ;
#77445=ADVANCED_FACE ( 'NONE', ( #41940 ), #28605, .T. ) ;
#77491=EDGE_LOOP ( 'NONE', ( #110329, #88622, #78756, #34639, #78432 ) ) ;
#77540=DIRECTION ( 'NONE',  ( 0.000000000000000000, -1.000000000000000000, 0.000000000000000000 ) ) ;
#77656=SURFACE_STYLE_USAGE ( .BOTH. , #17710 ) ;
#77734=EDGE_CURVE ( 'NONE', #6510, #57665, #24463, .T. ) ;
#77779=CIRCLE ( 'NONE', #52770, 2.000000000000001776 ) ;
#78432=ORIENTED_EDGE ( 'NONE', *, *, #15257, .F. ) ;
#78461=DIRECTION ( 'NONE',  ( 0.000000000000000000, 0.000000000000000000, 1.000000000000000000 ) ) ;
#78469=SPHERICAL_SURFACE ( 'NONE', #39205, 7.299999999999999822 ) ;
#78589=AXIS2_PLACEMENT_3D ( 'NONE', #61475, #88311, #11604 ) ;
#78756=ORIENTED_EDGE ( 'NONE', *, *, #42604, .F. ) ;
#78773=CARTESIAN_POINT ( 'NONE',  ( -111.9617233841873940, 1305.913060387289988, 301.5890982715878863 ) ) ;
#78778=CARTESIAN_POINT ( 'NONE',  ( -112.0992599419676452, 1391.413060387289988, 306.3568108987562937 ) ) ;
#79764=AXIS2_PLACEMENT_3D ( 'NONE', #41972, #76671, #83963 ) ;
#79812=SURFACE_SIDE_STYLE ('',( #54079 ) ) ;
#79949=CARTESIAN_POINT ( 'NONE',  ( -113.4000000000000057, 1392.913060387289988, 304.2218459572590064 ) ) ;
#80015=VECTOR ( 'NONE', #102582, 1000.000000000000000 ) ;
#80074=DIRECTION ( 'NONE',  ( 0.000000000000000000, 0.000000000000000000, 1.000000000000000000 ) ) ;
#80423=PRODUCT_DEFINITION_CONTEXT ( 'detailed design', #39875, 'design' ) ;
#80901=( LENGTH_UNIT ( ) NAMED_UNIT ( * ) SI_UNIT ( .MILLI., .METRE. ) );
#80977=CYLINDRICAL_SURFACE ( 'NONE', #65372, 2.499999999999989786 ) ;
#81271=CARTESIAN_POINT ( 'NONE',  ( -113.4000000000000057, 1304.231242809270043, 304.2218459572590064 ) ) ;
#82275=TOROIDAL_SURFACE ( 'NONE', #53705, 3.000000000000000000, 0.5000000000000000000 ) ;
#82922=PRODUCT_DEFINITION ( 'UNKNOWN', '', #38682, #80423 ) ;
#82952=ORIENTED_EDGE ( 'NONE', *, *, #65494, .T. ) ;
#83101=EDGE_CURVE ( 'NONE', #22154, #44485, #30140, .T. ) ;
#83410=CARTESIAN_POINT ( 'NONE',  ( -113.4000000000000057, 1305.913060387289988, 304.2218459572590064 ) ) ;
#83963=DIRECTION ( 'NONE',  ( 0.4794255386042027833, 0.000000000000000000, -0.8775825618903728698 ) ) ;
#84615=ORIENTED_EDGE ( 'NONE', *, *, #17086, .T. ) ;
#84698=DIRECTION ( 'NONE',  ( 0.000000000000000000, -1.000000000000000000, 0.000000000000000000 ) ) ;
#84956=CIRCLE ( 'NONE', #56381, 2.500000000000002220 ) ;
#85159=SHAPE_DEFINITION_REPRESENTATION ( #72391, #110199 ) ;
#86378=FACE_OUTER_BOUND ( 'NONE', #43604, .T. ) ;
#86694=DIRECTION ( 'NONE',  ( -6.498030146439999846E-14, -1.000000000000000000, -7.271071663860000024E-13 ) ) ;
#86924=DIRECTION ( 'NONE',  ( -0.2254368866615512057, -0.7071067811873372744, 0.6702075873423324337 ) ) ;
#87082=CARTESIAN_POINT ( 'NONE',  ( -113.4000000000000057, 1310.214785017039958, 304.2218459572619622 ) ) ;
#87268=VERTEX_POINT ( 'NONE', #78773 ) ;
#88204=( NAMED_UNIT ( * ) SI_UNIT ( $, .STERADIAN. ) SOLID_ANGLE_UNIT ( ) );
#88311=DIRECTION ( 'NONE',  ( 0.000000000000000000, 1.000000000000000000, 0.000000000000000000 ) ) ;
#88444=LINE ( 'NONE', #36377, #47259 ) ;
#88622=ORIENTED_EDGE ( 'NONE', *, *, #6879, .T. ) ;
#89036=ADVANCED_FACE ( 'NONE', ( #50450, #91876 ), #8970, .F. ) ;
#89623=AXIS2_PLACEMENT_3D ( 'NONE', #67478, #14831, #49020 ) ;
#89675=AXIS2_PLACEMENT_3D ( 'NONE', #652, #36982, #1762 ) ;
#89891=CARTESIAN_POINT ( 'NONE',  ( -113.4000000000000057, 1305.913060387289988, 304.2218459572590064 ) ) ;
#90192=ORIENTED_EDGE ( 'NONE', *, *, #68636, .T. ) ;
#90447=EDGE_LOOP ( 'NONE', ( #49340, #105453, #5350, #41160, #66564 ) ) ;
#90796=AXIS2_PLACEMENT_3D ( 'NONE', #62895, #36533, #37081 ) ;
#91183=AXIS2_PLACEMENT_3D ( 'NONE', #93982, #86694, #8868 ) ;
#91318=CARTESIAN_POINT ( 'NONE',  ( -111.0888070733315516, 1304.231242809270043, 299.9912356824837616 ) ) ;
#91555=DIRECTION ( 'NONE',  ( 0.4794255386042019507, 0.000000000000000000, -0.8775825618903732028 ) ) ;
#91876=FACE_OUTER_BOUND ( 'NONE', #23373, .T. ) ;
#92151=ORIENTED_EDGE ( 'NONE', *, *, #65494, .F. ) ;
#92243=AXIS2_PLACEMENT_3D ( 'NONE', #64667, #98785, #22047 ) ;
#92289=CARTESIAN_POINT ( 'NONE',  ( -113.4000000000000057, 1391.913060387289988, 306.7218459572590064 ) ) ;
#92458=ORIENTED_EDGE ( 'NONE', *, *, #53718, .T. ) ;
#92737=AXIS2_PLACEMENT_3D ( 'NONE', #45399, #29664, #80074 ) ;
#92794=DIRECTION ( 'NONE',  ( 0.000000000000000000, 0.000000000000000000, 1.000000000000000000 ) ) ;
#92914=DIRECTION ( 'NONE',  ( 0.000000000000000000, 0.000000000000000000, 1.000000000000000000 ) ) ;
#93103=CYLINDRICAL_SURFACE ( 'NONE', #62474, 2.499999999999989786 ) ;
#93217=CIRCLE ( 'NONE', #34237, 7.300000000000009592 ) ;
#93224=AXIS2_PLACEMENT_3D ( 'NONE', #68597, #77540, #103256 ) ;
#93377=DIRECTION ( 'NONE',  ( -0.8775825618903712044, -0.000000000000000000, -0.4794255386042061140 ) ) ;
#93758=DIRECTION ( 'NONE',  ( 0.000000000000000000, -1.000000000000000000, 0.000000000000000000 ) ) ;
#93867=EDGE_CURVE ( 'NONE', #10690, #96166, #109451, .T. ) ;
#93982=CARTESIAN_POINT ( 'NONE',  ( -113.4000000000000057, 1310.214785017039958, 304.2218459572619622 ) ) ;
#94097=VERTEX_POINT ( 'NONE', #110169 ) ;
#94626=EDGE_CURVE ( 'NONE', #57348, #94097, #100319, .T. ) ;
#94637=DIRECTION ( 'NONE',  ( 0.000000000000000000, -1.000000000000000000, 0.000000000000000000 ) ) ;
#95038=CONICAL_SURFACE ( 'NONE', #89675, 0.9999999999999910072, 0.7853981633970000820 ) ;
#95846=AXIS2_PLACEMENT_3D ( 'NONE', #102791, #41802, #9858 ) ;
#96077=CIRCLE ( 'NONE', #103173, 0.5000000000000147660 ) ;
#96166=VERTEX_POINT ( 'NONE', #106600 ) ;
#96407=TOROIDAL_SURFACE ( 'NONE', #78589, 3.500000000000000000, 2.000000000000000000 ) ;
#96805=EDGE_CURVE ( 'NONE', #67505, #45568, #65722, .T. ) ;
#96852=DIRECTION ( 'NONE',  ( -0.4794255386042019507, 0.000000000000000000, 0.8775825618903732028 ) ) ;
#97665=EDGE_CURVE ( 'NONE', #106581, #10690, #33736, .T. ) ;
#97888=EDGE_CURVE ( 'NONE', #87268, #94097, #96077, .T. ) ;
#97904=FACE_OUTER_BOUND ( 'NONE', #12415, .T. ) ;
#98479=CARTESIAN_POINT ( 'NONE',  ( -113.4000000000000057, 1309.713060387289943, 304.2218459572590064 ) ) ;
#98514=ADVANCED_FACE ( 'NONE', ( #86378 ), #9664, .T. ) ;
#98666=ORIENTED_EDGE ( 'NONE', *, *, #28861, .F. ) ;
#98785=DIRECTION ( 'NONE',  ( 0.000000000000000000, -1.000000000000000000, 0.000000000000000000 ) ) ;
#99040=DIRECTION ( 'NONE',  ( 0.4794255386042096112, 0.000000000000000000, -0.8775825618903690950 ) ) ;
#99311=ADVANCED_FACE ( 'NONE', ( #105149 ), #65800, .T. ) ;
#100095=ADVANCED_BREP_SHAPE_REPRESENTATION ( '', ( #7937, #21632 ), #107481 ) ;
#100214=CIRCLE ( 'NONE', #43000, 4.820754716980014010 ) ;
#100283=CARTESIAN_POINT ( 'NONE',  ( -113.4000000000000057, 1305.913060387289988, 309.7218459572590064 ) ) ;
#100319=CIRCLE ( 'NONE', #9125, 2.500000000000002220 ) ;
#100697=CARTESIAN_POINT ( 'NONE',  ( -113.4000000000000057, 1306.413060387289988, 304.2218459572590064 ) ) ;
#101047=CIRCLE ( 'NONE', #18801, 2.500000000000002220 ) ;
#101092=CARTESIAN_POINT ( 'NONE',  ( -114.5985638465105154, 1306.413060387289988, 306.4158023619849018 ) ) ;
#102125=DIRECTION ( 'NONE',  ( 0.000000000000000000, 0.000000000000000000, 1.000000000000000000 ) ) ;
#102214=EDGE_CURVE ( 'NONE', #44485, #57348, #29661, .T. ) ;
#102225=( NAMED_UNIT ( * ) PLANE_ANGLE_UNIT ( ) SI_UNIT ( $, .RADIAN. ) );
#102542=VERTEX_POINT ( 'NONE', #19473 ) ;
#102582=DIRECTION ( 'NONE',  ( 0.2254368866614593903, -0.7071067811863919195, -0.6702075873433606112 ) ) ;
#102749=DIRECTION ( 'NONE',  ( -6.498030146439999846E-14, -1.000000000000000000, -7.271071663860000024E-13 ) ) ;
#102791=CARTESIAN_POINT ( 'NONE',  ( -114.8382766158126174, 1306.413060387289988, 306.8545936429301264 ) ) ;
#103001=ORIENTED_EDGE ( 'NONE', *, *, #42604, .T. ) ;
#103015=ORIENTED_EDGE ( 'NONE', *, *, #65289, .F. ) ;
#103083=CARTESIAN_POINT ( 'NONE',  ( -113.4000000000000057, 1306.413060387289988, 304.2218459572590064 ) ) ;
#103173=AXIS2_PLACEMENT_3D ( 'NONE', #66568, #93377, #23419 ) ;
#103256=DIRECTION ( 'NONE',  ( 0.000000000000000000, 0.000000000000000000, 1.000000000000000000 ) ) ;
#103632=EDGE_LOOP ( 'NONE', ( #107474, #45054 ) ) ;
#104478=AXIS2_PLACEMENT_3D ( 'NONE', #59542, #67958, #110482 ) ;
#104998=SURFACE_STYLE_USAGE ( .BOTH. , #79812 ) ;
#105149=FACE_OUTER_BOUND ( 'NONE', #90447, .T. ) ;
#105453=ORIENTED_EDGE ( 'NONE', *, *, #63708, .T. ) ;
#105479=AXIS2_PLACEMENT_3D ( 'NONE', #92289, #49210, #6634 ) ;
#105550=ORIENTED_EDGE ( 'NONE', *, *, #28297, .T. ) ;
#105668=ORIENTED_EDGE ( 'NONE', *, *, #54007, .F. ) ;
#105789=CARTESIAN_POINT ( 'NONE',  ( -113.4000000000000057, 1305.733110638860126, 304.2218459572590064 ) ) ;
#106386=AXIS2_PLACEMENT_3D ( 'NONE', #5590, #31881, #108031 ) ;
#106436=CARTESIAN_POINT ( 'NONE',  ( -113.9202960232132540, 1392.913060387289988, 303.3678599806595457 ) ) ;
#106581=VERTEX_POINT ( 'NONE', #67808 ) ;
#106600=CARTESIAN_POINT ( 'NONE',  ( -110.7631994250367029, 1305.714868215269917, 299.3952148801843691 ) ) ;
#107356=ORIENTED_EDGE ( 'NONE', *, *, #96805, .F. ) ;
#107474=ORIENTED_EDGE ( 'NONE', *, *, #53718, .F. ) ;
#107481=( GEOMETRIC_REPRESENTATION_CONTEXT ( 3 ) GLOBAL_UNCERTAINTY_ASSIGNED_CONTEXT ( ( #67071 ) ) GLOBAL_UNIT_ASSIGNED_CONTEXT ( ( #33917, #102225, #60247 ) ) REPRESENTATION_CONTEXT ( 'NONE', 'WORKASPACE' ) );
#107518=ORIENTED_EDGE ( 'NONE', *, *, #24331, .F. ) ;
#108015=CARTESIAN_POINT ( 'NONE',  ( -114.5985638465105154, 1347.163060387289988, 306.4158023619849018 ) ) ;
#108031=DIRECTION ( 'NONE',  ( 0.000000000000000000, 0.000000000000000000, 1.000000000000000000 ) ) ;
#108812=DIRECTION ( 'NONE',  ( -0.4794255386042076128, 0.000000000000000000, 0.8775825618903700942 ) ) ;
#108906=DIRECTION ( 'NONE',  ( 0.000000000000000000, 1.000000000000000000, 0.000000000000000000 ) ) ;
#109451=CIRCLE ( 'NONE', #66543, 5.499916801759985319 ) ;
#109535=CARTESIAN_POINT ( 'NONE',  ( -114.5985638465105154, 1391.413060387289988, 306.4158023619849018 ) ) ;
#109547=ORIENTED_EDGE ( 'NONE', *, *, #96805, .T. ) ;
#110010=CARTESIAN_POINT ( 'NONE',  ( -113.4000000000000057, 1309.713060387289943, 304.2218459572590064 ) ) ;
#110085=CARTESIAN_POINT ( 'NONE',  ( 0.000000000000000000, 0.000000000000000000, 0.000000000000000000 ) ) ;
#110086=DIRECTION ( 'NONE',  ( 0.000000000000000000, -1.000000000000000000, 0.000000000000000000 ) ) ;
#110147=CIRCLE ( 'NONE', #92243, 5.301724629749982043 ) ;
#110149=FILL_AREA_STYLE ('',( #10448 ) ) ;
#110169=CARTESIAN_POINT ( 'NONE',  ( -112.2014361534894817, 1306.413060387289988, 302.0278895525330540 ) ) ;
#110190=DIRECTION ( 'NONE',  ( 0.000000000000000000, -1.000000000000000000, 0.000000000000000000 ) ) ;
#110199=SHAPE_REPRESENTATION ( 'Handle Mounting Screw', ( #21632 ), #107481 ) ;
#110240=DIRECTION ( 'NONE',  ( 0.000000000000000000, 0.000000000000000000, 1.000000000000000000 ) ) ;
#110329=ORIENTED_EDGE ( 'NONE', *, *, #28861, .T. ) ;
#110482=DIRECTION ( 'NONE',  ( 0.000000000000000000, 0.000000000000000000, 1.000000000000000000 ) ) ;
#110528=ORIENTED_EDGE ( 'NONE', *, *, #54069, .F. ) ;
#110698=( LENGTH_UNIT ( ) NAMED_UNIT ( * ) SI_UNIT ( .MILLI., .METRE. ) );
ENDSEC;
END-ISO-10303-21;
